ISO-10303-21;
HEADER;
/* Generated by software containing ST-Developer
 * from STEP Tools, Inc. (www.steptools.com) 
 */

FILE_DESCRIPTION(
/* description */ ('Manual piston pump'),
/* implementation_level */ '2;1');

FILE_NAME(
/* name */ 'Cap Screw - M4x16.step',
/* time_stamp */ '2026-11-02T16:54:23-08:00',
/* author */ (''),
/* organization */ (''),
/* preprocessor_version */ 'ST-DEVELOPER v20.2',
/* originating_system */ 'Autodesk Translation Framework v15.17.0.0',
/* authorisation */ '');

FILE_SCHEMA (('AUTOMOTIVE_DESIGN { 1 0 10303 214 3 1 1 }'));
ENDSEC;

DATA;
#10=MECHANICAL_DESIGN_GEOMETRIC_PRESENTATION_REPRESENTATION('',(#743),#19043);
#525=ORIENTED_CLOSED_SHELL('',*,#9531,.F.);
#544=CONICAL_SURFACE('',#11163,0.325,0.785398163397448);
#545=CONICAL_SURFACE('',#11167,0.335,0.785398163397448);
#546=CONICAL_SURFACE('',#11171,0.21,0.463647609000806);
#547=CONICAL_SURFACE('',#11175,0.18,0.785398163397448);
#556=BREP_WITH_VOIDS('Body1',#9530,(#525));
#609=SHAPE_REPRESENTATION_RELATIONSHIP('SRR','None',#19358,#672);
#672=ADVANCED_BREP_SHAPE_REPRESENTATION('',(#556),#19025);
#743=STYLED_ITEM('',(#19663),#556);
#1019=FACE_BOUND('',#2518,.T.);
#1254=CYLINDRICAL_SURFACE('',#11165,0.35);
#1255=CYLINDRICAL_SURFACE('',#11173,0.1954);
#1746=FACE_OUTER_BOUND('',#2513,.T.);
#1747=FACE_OUTER_BOUND('',#2514,.T.);
#1748=FACE_OUTER_BOUND('',#2515,.T.);
#1749=FACE_OUTER_BOUND('',#2516,.T.);
#1750=FACE_OUTER_BOUND('',#2517,.T.);
#1751=FACE_OUTER_BOUND('',#2519,.T.);
#1752=FACE_OUTER_BOUND('',#2520,.T.);
#1753=FACE_OUTER_BOUND('',#2521,.T.);
#1754=FACE_OUTER_BOUND('',#2522,.T.);
#1755=FACE_OUTER_BOUND('',#2523,.T.);
#1756=FACE_OUTER_BOUND('',#2524,.T.);
#1757=FACE_OUTER_BOUND('',#2525,.T.);
#1758=FACE_OUTER_BOUND('',#2526,.T.);
#1759=FACE_OUTER_BOUND('',#2527,.T.);
#1760=FACE_OUTER_BOUND('',#2528,.T.);
#1761=FACE_OUTER_BOUND('',#2529,.T.);
#1762=FACE_OUTER_BOUND('',#2530,.T.);
#2513=EDGE_LOOP('',(#8103));
#2514=EDGE_LOOP('',(#8104,#8105,#8106,#8107));
#2515=EDGE_LOOP('',(#8108,#8109,#8110,#8111));
#2516=EDGE_LOOP('',(#8112,#8113,#8114,#8115));
#2517=EDGE_LOOP('',(#8116));
#2518=EDGE_LOOP('',(#8117));
#2519=EDGE_LOOP('',(#8118,#8119,#8120,#8121));
#2520=EDGE_LOOP('',(#8122,#8123,#8124,#8125));
#2521=EDGE_LOOP('',(#8126,#8127,#8128,#8129));
#2522=EDGE_LOOP('',(#8130));
#2523=EDGE_LOOP('',(#8131,#8132,#8133,#8134));
#2524=EDGE_LOOP('',(#8135,#8136,#8137,#8138));
#2525=EDGE_LOOP('',(#8139,#8140,#8141,#8142));
#2526=EDGE_LOOP('',(#8143,#8144,#8145,#8146));
#2527=EDGE_LOOP('',(#8147,#8148,#8149,#8150));
#2528=EDGE_LOOP('',(#8151,#8152,#8153,#8154));
#2529=EDGE_LOOP('',(#8155,#8156,#8157,#8158,#8159,#8160));
#2530=EDGE_LOOP('',(#8161,#8162,#8163,#8164,#8165,#8166));
#3062=CIRCLE('',#11162,0.3);
#3063=CIRCLE('',#11164,0.35);
#3064=CIRCLE('',#11166,0.35);
#3065=CIRCLE('',#11168,0.32);
#3066=CIRCLE('',#11170,0.22);
#3067=CIRCLE('',#11172,0.1954);
#3068=CIRCLE('',#11174,0.1954);
#3069=CIRCLE('',#11176,0.16);
#3615=LINE('',#18161,#4219);
#3616=LINE('',#18165,#4220);
#3617=LINE('',#18169,#4221);
#3618=LINE('',#18176,#4222);
#3619=LINE('',#18180,#4223);
#3620=LINE('',#18184,#4224);
#3621=LINE('',#18189,#4225);
#3622=LINE('',#18191,#4226);
#3623=LINE('',#18193,#4227);
#3624=LINE('',#18194,#4228);
#3625=LINE('',#18197,#4229);
#3626=LINE('',#18199,#4230);
#3627=LINE('',#18200,#4231);
#3628=LINE('',#18203,#4232);
#3629=LINE('',#18205,#4233);
#3630=LINE('',#18206,#4234);
#3631=LINE('',#18209,#4235);
#3632=LINE('',#18211,#4236);
#3633=LINE('',#18212,#4237);
#3634=LINE('',#18215,#4238);
#3635=LINE('',#18217,#4239);
#3636=LINE('',#18218,#4240);
#3637=LINE('',#18220,#4241);
#3638=LINE('',#18221,#4242);
#4219=VECTOR('',#13807,0.325);
#4220=VECTOR('',#13812,0.35);
#4221=VECTOR('',#13817,0.335);
#4222=VECTOR('',#13826,0.21);
#4223=VECTOR('',#13831,0.2);
#4224=VECTOR('',#13836,0.18);
#4225=VECTOR('',#13841,1.);
#4226=VECTOR('',#13842,1.);
#4227=VECTOR('',#13843,1.);
#4228=VECTOR('',#13844,1.);
#4229=VECTOR('',#13847,1.);
#4230=VECTOR('',#13848,1.);
#4231=VECTOR('',#13849,1.);
#4232=VECTOR('',#13852,1.);
#4233=VECTOR('',#13853,1.);
#4234=VECTOR('',#13854,1.);
#4235=VECTOR('',#13857,1.);
#4236=VECTOR('',#13858,1.);
#4237=VECTOR('',#13859,1.);
#4238=VECTOR('',#13862,1.);
#4239=VECTOR('',#13863,1.);
#4240=VECTOR('',#13864,1.);
#4241=VECTOR('',#13867,1.);
#4242=VECTOR('',#13868,1.);
#4970=VERTEX_POINT('',#18156);
#4971=VERTEX_POINT('',#18159);
#4972=VERTEX_POINT('',#18163);
#4973=VERTEX_POINT('',#18167);
#4974=VERTEX_POINT('',#18171);
#4975=VERTEX_POINT('',#18174);
#4976=VERTEX_POINT('',#18178);
#4977=VERTEX_POINT('',#18182);
#4978=VERTEX_POINT('',#18187);
#4979=VERTEX_POINT('',#18188);
#4980=VERTEX_POINT('',#18190);
#4981=VERTEX_POINT('',#18192);
#4982=VERTEX_POINT('',#18196);
#4983=VERTEX_POINT('',#18198);
#4984=VERTEX_POINT('',#18202);
#4985=VERTEX_POINT('',#18204);
#4986=VERTEX_POINT('',#18208);
#4987=VERTEX_POINT('',#18210);
#4988=VERTEX_POINT('',#18214);
#4989=VERTEX_POINT('',#18216);
#6038=EDGE_CURVE('',#4970,#4970,#3062,.T.);
#6039=EDGE_CURVE('',#4971,#4971,#3063,.T.);
#6040=EDGE_CURVE('',#4971,#4970,#3615,.T.);
#6041=EDGE_CURVE('',#4972,#4972,#3064,.T.);
#6042=EDGE_CURVE('',#4972,#4971,#3616,.T.);
#6043=EDGE_CURVE('',#4973,#4973,#3065,.T.);
#6044=EDGE_CURVE('',#4973,#4972,#3617,.T.);
#6045=EDGE_CURVE('',#4974,#4974,#3066,.T.);
#6046=EDGE_CURVE('',#4975,#4975,#3067,.F.);
#6047=EDGE_CURVE('',#4975,#4974,#3618,.T.);
#6048=EDGE_CURVE('',#4976,#4976,#3068,.F.);
#6049=EDGE_CURVE('',#4976,#4975,#3619,.T.);
#6050=EDGE_CURVE('',#4977,#4977,#3069,.T.);
#6051=EDGE_CURVE('',#4977,#4976,#3620,.T.);
#6052=EDGE_CURVE('',#4978,#4979,#3621,.T.);
#6053=EDGE_CURVE('',#4979,#4980,#3622,.T.);
#6054=EDGE_CURVE('',#4980,#4981,#3623,.T.);
#6055=EDGE_CURVE('',#4978,#4981,#3624,.T.);
#6056=EDGE_CURVE('',#4979,#4982,#3625,.T.);
#6057=EDGE_CURVE('',#4982,#4983,#3626,.T.);
#6058=EDGE_CURVE('',#4983,#4980,#3627,.T.);
#6059=EDGE_CURVE('',#4982,#4984,#3628,.T.);
#6060=EDGE_CURVE('',#4984,#4985,#3629,.T.);
#6061=EDGE_CURVE('',#4985,#4983,#3630,.T.);
#6062=EDGE_CURVE('',#4984,#4986,#3631,.T.);
#6063=EDGE_CURVE('',#4986,#4987,#3632,.T.);
#6064=EDGE_CURVE('',#4987,#4985,#3633,.T.);
#6065=EDGE_CURVE('',#4986,#4988,#3634,.T.);
#6066=EDGE_CURVE('',#4988,#4989,#3635,.T.);
#6067=EDGE_CURVE('',#4989,#4987,#3636,.T.);
#6068=EDGE_CURVE('',#4988,#4978,#3637,.T.);
#6069=EDGE_CURVE('',#4981,#4989,#3638,.T.);
#8103=ORIENTED_EDGE('',*,*,#6038,.F.);
#8104=ORIENTED_EDGE('',*,*,#6039,.F.);
#8105=ORIENTED_EDGE('',*,*,#6040,.T.);
#8106=ORIENTED_EDGE('',*,*,#6038,.T.);
#8107=ORIENTED_EDGE('',*,*,#6040,.F.);
#8108=ORIENTED_EDGE('',*,*,#6041,.F.);
#8109=ORIENTED_EDGE('',*,*,#6042,.T.);
#8110=ORIENTED_EDGE('',*,*,#6039,.T.);
#8111=ORIENTED_EDGE('',*,*,#6042,.F.);
#8112=ORIENTED_EDGE('',*,*,#6043,.F.);
#8113=ORIENTED_EDGE('',*,*,#6044,.T.);
#8114=ORIENTED_EDGE('',*,*,#6041,.T.);
#8115=ORIENTED_EDGE('',*,*,#6044,.F.);
#8116=ORIENTED_EDGE('',*,*,#6043,.T.);
#8117=ORIENTED_EDGE('',*,*,#6045,.F.);
#8118=ORIENTED_EDGE('',*,*,#6046,.F.);
#8119=ORIENTED_EDGE('',*,*,#6047,.T.);
#8120=ORIENTED_EDGE('',*,*,#6045,.T.);
#8121=ORIENTED_EDGE('',*,*,#6047,.F.);
#8122=ORIENTED_EDGE('',*,*,#6048,.F.);
#8123=ORIENTED_EDGE('',*,*,#6049,.T.);
#8124=ORIENTED_EDGE('',*,*,#6046,.T.);
#8125=ORIENTED_EDGE('',*,*,#6049,.F.);
#8126=ORIENTED_EDGE('',*,*,#6050,.F.);
#8127=ORIENTED_EDGE('',*,*,#6051,.T.);
#8128=ORIENTED_EDGE('',*,*,#6048,.T.);
#8129=ORIENTED_EDGE('',*,*,#6051,.F.);
#8130=ORIENTED_EDGE('',*,*,#6050,.T.);
#8131=ORIENTED_EDGE('',*,*,#6052,.T.);
#8132=ORIENTED_EDGE('',*,*,#6053,.T.);
#8133=ORIENTED_EDGE('',*,*,#6054,.T.);
#8134=ORIENTED_EDGE('',*,*,#6055,.F.);
#8135=ORIENTED_EDGE('',*,*,#6056,.T.);
#8136=ORIENTED_EDGE('',*,*,#6057,.T.);
#8137=ORIENTED_EDGE('',*,*,#6058,.T.);
#8138=ORIENTED_EDGE('',*,*,#6053,.F.);
#8139=ORIENTED_EDGE('',*,*,#6059,.T.);
#8140=ORIENTED_EDGE('',*,*,#6060,.T.);
#8141=ORIENTED_EDGE('',*,*,#6061,.T.);
#8142=ORIENTED_EDGE('',*,*,#6057,.F.);
#8143=ORIENTED_EDGE('',*,*,#6062,.T.);
#8144=ORIENTED_EDGE('',*,*,#6063,.T.);
#8145=ORIENTED_EDGE('',*,*,#6064,.T.);
#8146=ORIENTED_EDGE('',*,*,#6060,.F.);
#8147=ORIENTED_EDGE('',*,*,#6065,.T.);
#8148=ORIENTED_EDGE('',*,*,#6066,.T.);
#8149=ORIENTED_EDGE('',*,*,#6067,.T.);
#8150=ORIENTED_EDGE('',*,*,#6063,.F.);
#8151=ORIENTED_EDGE('',*,*,#6068,.T.);
#8152=ORIENTED_EDGE('',*,*,#6055,.T.);
#8153=ORIENTED_EDGE('',*,*,#6069,.T.);
#8154=ORIENTED_EDGE('',*,*,#6066,.F.);
#8155=ORIENTED_EDGE('',*,*,#6068,.F.);
#8156=ORIENTED_EDGE('',*,*,#6065,.F.);
#8157=ORIENTED_EDGE('',*,*,#6062,.F.);
#8158=ORIENTED_EDGE('',*,*,#6059,.F.);
#8159=ORIENTED_EDGE('',*,*,#6056,.F.);
#8160=ORIENTED_EDGE('',*,*,#6052,.F.);
#8161=ORIENTED_EDGE('',*,*,#6069,.F.);
#8162=ORIENTED_EDGE('',*,*,#6054,.F.);
#8163=ORIENTED_EDGE('',*,*,#6058,.F.);
#8164=ORIENTED_EDGE('',*,*,#6061,.F.);
#8165=ORIENTED_EDGE('',*,*,#6064,.F.);
#8166=ORIENTED_EDGE('',*,*,#6067,.F.);
#8823=PLANE('',#11161);
#8824=PLANE('',#11169);
#8825=PLANE('',#11177);
#8826=PLANE('',#11178);
#8827=PLANE('',#11179);
#8828=PLANE('',#11180);
#8829=PLANE('',#11181);
#8830=PLANE('',#11182);
#8831=PLANE('',#11183);
#8832=PLANE('',#11184);
#8833=PLANE('',#11185);
#9351=ADVANCED_FACE('',(#1746),#8823,.T.);
#9352=ADVANCED_FACE('',(#1747),#544,.T.);
#9353=ADVANCED_FACE('',(#1748),#1254,.T.);
#9354=ADVANCED_FACE('',(#1749),#545,.T.);
#9355=ADVANCED_FACE('',(#1750,#1019),#8824,.T.);
#9356=ADVANCED_FACE('',(#1751),#546,.T.);
#9357=ADVANCED_FACE('',(#1752),#1255,.T.);
#9358=ADVANCED_FACE('',(#1753),#547,.T.);
#9359=ADVANCED_FACE('',(#1754),#8825,.T.);
#9360=ADVANCED_FACE('',(#1755),#8826,.F.);
#9361=ADVANCED_FACE('',(#1756),#8827,.F.);
#9362=ADVANCED_FACE('',(#1757),#8828,.F.);
#9363=ADVANCED_FACE('',(#1758),#8829,.F.);
#9364=ADVANCED_FACE('',(#1759),#8830,.F.);
#9365=ADVANCED_FACE('',(#1760),#8831,.F.);
#9366=ADVANCED_FACE('',(#1761),#8832,.F.);
#9367=ADVANCED_FACE('',(#1762),#8833,.F.);
#9530=CLOSED_SHELL('',(#9351,#9352,#9353,#9354,#9355,#9356,#9357,#9358,
#9359));
#9531=CLOSED_SHELL('',(#9360,#9361,#9362,#9363,#9364,#9365,#9366,#9367));
#11160=AXIS2_PLACEMENT_3D('',#18154,#13797,#13798);
#11161=AXIS2_PLACEMENT_3D('',#18155,#13799,#13800);
#11162=AXIS2_PLACEMENT_3D('',#18157,#13801,#13802);
#11163=AXIS2_PLACEMENT_3D('',#18158,#13803,#13804);
#11164=AXIS2_PLACEMENT_3D('',#18160,#13805,#13806);
#11165=AXIS2_PLACEMENT_3D('',#18162,#13808,#13809);
#11166=AXIS2_PLACEMENT_3D('',#18164,#13810,#13811);
#11167=AXIS2_PLACEMENT_3D('',#18166,#13813,#13814);
#11168=AXIS2_PLACEMENT_3D('',#18168,#13815,#13816);
#11169=AXIS2_PLACEMENT_3D('',#18170,#13818,#13819);
#11170=AXIS2_PLACEMENT_3D('',#18172,#13820,#13821);
#11171=AXIS2_PLACEMENT_3D('',#18173,#13822,#13823);
#11172=AXIS2_PLACEMENT_3D('',#18175,#13824,#13825);
#11173=AXIS2_PLACEMENT_3D('',#18177,#13827,#13828);
#11174=AXIS2_PLACEMENT_3D('',#18179,#13829,#13830);
#11175=AXIS2_PLACEMENT_3D('',#18181,#13832,#13833);
#11176=AXIS2_PLACEMENT_3D('',#18183,#13834,#13835);
#11177=AXIS2_PLACEMENT_3D('',#18185,#13837,#13838);
#11178=AXIS2_PLACEMENT_3D('',#18186,#13839,#13840);
#11179=AXIS2_PLACEMENT_3D('',#18195,#13845,#13846);
#11180=AXIS2_PLACEMENT_3D('',#18201,#13850,#13851);
#11181=AXIS2_PLACEMENT_3D('',#18207,#13855,#13856);
#11182=AXIS2_PLACEMENT_3D('',#18213,#13860,#13861);
#11183=AXIS2_PLACEMENT_3D('',#18219,#13865,#13866);
#11184=AXIS2_PLACEMENT_3D('',#18222,#13869,#13870);
#11185=AXIS2_PLACEMENT_3D('',#18223,#13871,#13872);
#13797=DIRECTION('axis',(0.,0.,1.));
#13798=DIRECTION('refdir',(1.,0.,0.));
#13799=DIRECTION('center_axis',(0.,1.,0.));
#13800=DIRECTION('ref_axis',(0.,0.,1.));
#13801=DIRECTION('center_axis',(0.,-1.,0.));
#13802=DIRECTION('ref_axis',(1.,0.,0.));
#13803=DIRECTION('center_axis',(0.,-1.,0.));
#13804=DIRECTION('ref_axis',(1.,0.,0.));
#13805=DIRECTION('center_axis',(0.,-1.,0.));
#13806=DIRECTION('ref_axis',(1.,0.,0.));
#13807=DIRECTION('',(0.707106781186547,0.707106781186548,8.65956056235493E-17));
#13808=DIRECTION('center_axis',(0.,-1.,0.));
#13809=DIRECTION('ref_axis',(1.,0.,0.));
#13810=DIRECTION('center_axis',(0.,-1.,0.));
#13811=DIRECTION('ref_axis',(1.,0.,0.));
#13812=DIRECTION('',(0.,1.,0.));
#13813=DIRECTION('center_axis',(0.,1.,0.));
#13814=DIRECTION('ref_axis',(1.,0.,0.));
#13815=DIRECTION('center_axis',(0.,-1.,0.));
#13816=DIRECTION('ref_axis',(1.,0.,0.));
#13817=DIRECTION('',(-0.707106781186547,0.707106781186548,-8.65956056235493E-17));
#13818=DIRECTION('center_axis',(0.,-1.,0.));
#13819=DIRECTION('ref_axis',(0.,0.,-1.));
#13820=DIRECTION('center_axis',(0.,-1.,0.));
#13821=DIRECTION('ref_axis',(1.,0.,0.));
#13822=DIRECTION('center_axis',(0.,1.,0.));
#13823=DIRECTION('ref_axis',(1.,0.,0.));
#13824=DIRECTION('center_axis',(0.,1.,0.));
#13825=DIRECTION('ref_axis',(1.,0.,0.));
#13826=DIRECTION('',(-0.447213595499958,0.894427190999916,-5.47678698264203E-17));
#13827=DIRECTION('center_axis',(0.,-1.,0.));
#13828=DIRECTION('ref_axis',(1.,0.,0.));
#13829=DIRECTION('center_axis',(0.,1.,0.));
#13830=DIRECTION('ref_axis',(1.,0.,0.));
#13831=DIRECTION('',(0.,1.,0.));
#13832=DIRECTION('center_axis',(0.,1.,0.));
#13833=DIRECTION('ref_axis',(1.,0.,0.));
#13834=DIRECTION('center_axis',(0.,-1.,0.));
#13835=DIRECTION('ref_axis',(1.,0.,0.));
#13836=DIRECTION('',(-0.707106781186547,0.707106781186548,-8.65956056235493E-17));
#13837=DIRECTION('center_axis',(0.,-1.,0.));
#13838=DIRECTION('ref_axis',(0.,0.,-1.));
#13839=DIRECTION('center_axis',(0.866025403784439,0.,-0.5));
#13840=DIRECTION('ref_axis',(0.5,0.,0.866025403784439));
#13841=DIRECTION('',(-0.5,0.,-0.866025403784439));
#13842=DIRECTION('',(0.,-1.,0.));
#13843=DIRECTION('',(0.5,0.,0.866025403784439));
#13844=DIRECTION('',(0.,-1.,0.));
#13845=DIRECTION('center_axis',(1.60246890531964E-16,0.,-1.));
#13846=DIRECTION('ref_axis',(1.,0.,1.60246890531964E-16));
#13847=DIRECTION('',(-1.,0.,-1.60246890531964E-16));
#13848=DIRECTION('',(0.,-1.,0.));
#13849=DIRECTION('',(1.,0.,1.60246890531964E-16));
#13850=DIRECTION('center_axis',(-0.866025403784439,0.,-0.5));
#13851=DIRECTION('ref_axis',(0.5,0.,-0.866025403784439));
#13852=DIRECTION('',(-0.5,0.,0.866025403784439));
#13853=DIRECTION('',(0.,-1.,0.));
#13854=DIRECTION('',(0.5,0.,-0.866025403784439));
#13855=DIRECTION('center_axis',(-0.866025403784439,0.,0.5));
#13856=DIRECTION('ref_axis',(-0.5,0.,-0.866025403784439));
#13857=DIRECTION('',(0.5,0.,0.866025403784439));
#13858=DIRECTION('',(0.,-1.,0.));
#13859=DIRECTION('',(-0.5,0.,-0.866025403784439));
#13860=DIRECTION('center_axis',(-1.60246890531964E-16,0.,1.));
#13861=DIRECTION('ref_axis',(-1.,0.,-1.60246890531964E-16));
#13862=DIRECTION('',(1.,0.,1.60246890531964E-16));
#13863=DIRECTION('',(0.,-1.,0.));
#13864=DIRECTION('',(-1.,0.,-1.60246890531964E-16));
#13865=DIRECTION('center_axis',(0.866025403784439,0.,0.5));
#13866=DIRECTION('ref_axis',(-0.5,0.,0.866025403784439));
#13867=DIRECTION('',(0.5,0.,-0.866025403784439));
#13868=DIRECTION('',(-0.5,0.,0.866025403784439));
#13869=DIRECTION('center_axis',(0.,1.,0.));
#13870=DIRECTION('ref_axis',(1.,0.,0.));
#13871=DIRECTION('center_axis',(0.,-1.,0.));
#13872=DIRECTION('ref_axis',(0.,0.,-1.));
#18154=CARTESIAN_POINT('',(0.,0.,0.));
#18155=CARTESIAN_POINT('Origin',(0.3,0.4,0.));
#18156=CARTESIAN_POINT('',(-0.3,0.4,-3.67394039744206E-17));
#18157=CARTESIAN_POINT('Origin',(0.,0.4,0.));
#18158=CARTESIAN_POINT('Origin',(0.,0.375,0.));
#18159=CARTESIAN_POINT('',(-0.35,0.35,-4.28626379701573E-17));
#18160=CARTESIAN_POINT('Origin',(0.,0.35,0.));
#18161=CARTESIAN_POINT('',(-0.325,0.375,-3.9801020972289E-17));
#18162=CARTESIAN_POINT('Origin',(0.,0.19,0.));
#18163=CARTESIAN_POINT('',(-0.35,0.03,-4.28626379701574E-17));
#18164=CARTESIAN_POINT('Origin',(0.,0.03,0.));
#18165=CARTESIAN_POINT('',(-0.35,0.19,-4.28626379701574E-17));
#18166=CARTESIAN_POINT('Origin',(0.,0.0149999999999999,0.));
#18167=CARTESIAN_POINT('',(-0.32,-3.29597460435593E-17,-3.91886975727153E-17));
#18168=CARTESIAN_POINT('Origin',(0.,0.,0.));
#18169=CARTESIAN_POINT('',(-0.335,0.0149999999999999,-4.10256677714363E-17));
#18170=CARTESIAN_POINT('Origin',(0.22,0.,0.));
#18171=CARTESIAN_POINT('',(-0.22,-6.93889390390723E-18,-2.69422295812418E-17));
#18172=CARTESIAN_POINT('Origin',(0.,0.,0.));
#18173=CARTESIAN_POINT('Origin',(0.,-0.02,0.));
#18174=CARTESIAN_POINT('',(-0.1954,-0.0492,2.39295984553393E-17));
#18175=CARTESIAN_POINT('Origin',(0.,-0.0492,0.));
#18176=CARTESIAN_POINT('',(-0.21,-0.02,-2.57175827820944E-17));
#18177=CARTESIAN_POINT('Origin',(0.,-0.8,0.));
#18178=CARTESIAN_POINT('',(-0.1954,-1.5646,2.39295984553393E-17));
#18179=CARTESIAN_POINT('Origin',(0.,-1.5646,0.));
#18180=CARTESIAN_POINT('',(-0.1954,-0.8,-2.39295984553393E-17));
#18181=CARTESIAN_POINT('Origin',(0.,-1.58,0.));
#18182=CARTESIAN_POINT('',(-0.16,-1.6,-1.95943487863577E-17));
#18183=CARTESIAN_POINT('Origin',(0.,-1.6,0.));
#18184=CARTESIAN_POINT('',(-0.18,-1.58,-2.20436423846524E-17));
#18185=CARTESIAN_POINT('Origin',(0.,-1.6,0.));
#18186=CARTESIAN_POINT('Origin',(0.0866025403784439,-0.4,-0.15));
#18187=CARTESIAN_POINT('',(0.173205080756888,-0.4,0.));
#18188=CARTESIAN_POINT('',(0.0866025403784439,-0.4,-0.15));
#18189=CARTESIAN_POINT('',(0.173205080756888,-0.4,0.));
#18190=CARTESIAN_POINT('',(0.0866025403784439,-0.64,-0.15));
#18191=CARTESIAN_POINT('',(0.0866025403784439,-0.4,-0.15));
#18192=CARTESIAN_POINT('',(0.173205080756888,-0.64,0.));
#18193=CARTESIAN_POINT('',(0.173205080756888,-0.64,0.));
#18194=CARTESIAN_POINT('',(0.173205080756888,-0.4,0.));
#18195=CARTESIAN_POINT('Origin',(-0.0866025403784438,-0.4,-0.15));
#18196=CARTESIAN_POINT('',(-0.0866025403784438,-0.4,-0.15));
#18197=CARTESIAN_POINT('',(0.0866025403784439,-0.4,-0.15));
#18198=CARTESIAN_POINT('',(-0.0866025403784438,-0.64,-0.15));
#18199=CARTESIAN_POINT('',(-0.0866025403784438,-0.4,-0.15));
#18200=CARTESIAN_POINT('',(0.0866025403784439,-0.64,-0.15));
#18201=CARTESIAN_POINT('Origin',(-0.173205080756888,-0.4,-2.77555756156289E-17));
#18202=CARTESIAN_POINT('',(-0.173205080756888,-0.4,-2.12115047744981E-17));
#18203=CARTESIAN_POINT('',(-0.0866025403784438,-0.4,-0.15));
#18204=CARTESIAN_POINT('',(-0.173205080756888,-0.64,-2.77555756156289E-17));
#18205=CARTESIAN_POINT('',(-0.173205080756888,-0.4,-2.12115047744981E-17));
#18206=CARTESIAN_POINT('',(-0.0866025403784438,-0.64,-0.15));
#18207=CARTESIAN_POINT('Origin',(-0.0866025403784439,-0.4,0.15));
#18208=CARTESIAN_POINT('',(-0.0866025403784439,-0.4,0.15));
#18209=CARTESIAN_POINT('',(-0.173205080756888,-0.4,-2.12115047744981E-17));
#18210=CARTESIAN_POINT('',(-0.0866025403784439,-0.64,0.15));
#18211=CARTESIAN_POINT('',(-0.0866025403784439,-0.4,0.15));
#18212=CARTESIAN_POINT('',(-0.173205080756888,-0.64,-2.12115047744981E-17));
#18213=CARTESIAN_POINT('Origin',(0.0866025403784439,-0.4,0.15));
#18214=CARTESIAN_POINT('',(0.0866025403784439,-0.4,0.15));
#18215=CARTESIAN_POINT('',(-0.0866025403784439,-0.4,0.15));
#18216=CARTESIAN_POINT('',(0.0866025403784439,-0.64,0.15));
#18217=CARTESIAN_POINT('',(0.0866025403784439,-0.4,0.15));
#18218=CARTESIAN_POINT('',(-0.0866025403784439,-0.64,0.15));
#18219=CARTESIAN_POINT('Origin',(0.173205080756888,-0.4,0.));
#18220=CARTESIAN_POINT('',(0.0866025403784439,-0.4,0.15));
#18221=CARTESIAN_POINT('',(0.0866025403784439,-0.64,0.15));
#18222=CARTESIAN_POINT('Origin',(0.,-0.4,-2.77555756156289E-17));
#18223=CARTESIAN_POINT('Origin',(0.,-0.64,-2.77555756156289E-17));
#18954=UNCERTAINTY_MEASURE_WITH_UNIT(LENGTH_MEASURE(0.001),#19044,
'DISTANCE_ACCURACY_VALUE',
'Maximum model space distance between geometric entities at asserted c
onnectivities');
#18972=UNCERTAINTY_MEASURE_WITH_UNIT(LENGTH_MEASURE(0.001),#19044,
'DISTANCE_ACCURACY_VALUE',
'Maximum model space distance between geometric entities at asserted c
onnectivities');
#19025=(
GEOMETRIC_REPRESENTATION_CONTEXT(3)
GLOBAL_UNCERTAINTY_ASSIGNED_CONTEXT((#18954))
GLOBAL_UNIT_ASSIGNED_CONTEXT((#19044,#19046,#19047))
REPRESENTATION_CONTEXT('','3D')
);
#19043=(
GEOMETRIC_REPRESENTATION_CONTEXT(3)
GLOBAL_UNCERTAINTY_ASSIGNED_CONTEXT((#18972))
GLOBAL_UNIT_ASSIGNED_CONTEXT((#19044,#19046,#19047))
REPRESENTATION_CONTEXT('','3D')
);
#19044=(
LENGTH_UNIT()
NAMED_UNIT(*)
SI_UNIT(.CENTI.,.METRE.)
);
#19046=(
NAMED_UNIT(*)
PLANE_ANGLE_UNIT()
SI_UNIT($,.RADIAN.)
);
#19047=(
NAMED_UNIT(*)
SI_UNIT($,.STERADIAN.)
SOLID_ANGLE_UNIT()
);
#19100=SHAPE_DEFINITION_REPRESENTATION(#19177,#19358);
#19177=PRODUCT_DEFINITION_SHAPE('',$,#19429);
#19358=SHAPE_REPRESENTATION('',(#11160),#19025);
#19376=PRODUCT_DEFINITION_CONTEXT('part definition',#19588,'design');
#19429=PRODUCT_DEFINITION('2026-11-03-00-38-46-497','Cap Screw - M4x16',
#19499,#19376);
#19499=PRODUCT_DEFINITION_FORMATION('',$,#19642);
#19588=APPLICATION_CONTEXT(
'Core Data for Automotive Mechanical Design Process');
#19589=PRODUCT_CONTEXT('part definition',#19588,'mechanical');
#19642=PRODUCT('2026-11-03-00-38-46-497','Cap Screw - M4x16',
'Cap Screw - M4x16',(#19589));
#19663=PRESENTATION_STYLE_ASSIGNMENT((#19669));
#19669=SURFACE_STYLE_USAGE(.BOTH.,#19675);
#19675=SURFACE_SIDE_STYLE('',(#19681));
#19681=SURFACE_STYLE_FILL_AREA(#19687);
#19687=FILL_AREA_STYLE('CAD Library Painted - Graphite',(#19693));
#19693=FILL_AREA_STYLE_COLOUR('CAD Library Painted - Graphite',#19699);
#19699=COLOUR_RGB('CAD Library Painted - Graphite',0.168627450980392,0.192156862745098,
0.231372549019608);
ENDSEC;
END-ISO-10303-21;
